ISO-10303-21;
HEADER;
/* Generated by software containing ST-Developer
 * from STEP Tools, Inc. (www.steptools.com) 
 */

FILE_DESCRIPTION(
/* description */ (''),
/* implementation_level */ '2;1');

FILE_NAME(
/* name */ 'Front_Block_02.step',
/* time_stamp */ '2026-10-23T22:30:33+06:00',
/* author */ (''),
/* organization */ (''),
/* preprocessor_version */ 'ST-DEVELOPER v20.2',
/* originating_system */ 'Autodesk Translation Framework v15.15.0.0',
/* authorisation */ '');

FILE_SCHEMA (('AUTOMOTIVE_DESIGN { 1 0 10303 214 3 1 1 }'));
ENDSEC;

DATA;
#10=MECHANICAL_DESIGN_GEOMETRIC_PRESENTATION_REPRESENTATION('',(#239),#10131);
#99=ELLIPSE('',#6268,1.0823922002924,1.);
#100=ELLIPSE('',#6269,1.0823922002924,1.);
#101=ELLIPSE('',#6271,1.08239220029239,1.);
#102=ELLIPSE('',#6273,1.0823922002924,1.);
#103=ELLIPSE('',#6275,1.08239220029239,1.);
#104=ELLIPSE('',#6277,1.0823922002924,1.);
#105=ELLIPSE('',#6279,1.0823922002924,1.);
#106=ELLIPSE('',#6281,1.08239220029239,1.);
#107=ELLIPSE('',#6289,1.0823922002924,1.);
#108=ELLIPSE('',#6290,1.08239220029239,1.);
#109=ELLIPSE('',#6292,1.08239220029239,1.);
#110=ELLIPSE('',#6294,1.08239220029239,1.);
#111=ELLIPSE('',#6296,1.08239220029239,1.);
#112=ELLIPSE('',#6298,1.0823922002924,1.);
#113=ELLIPSE('',#6300,1.08239220029239,1.);
#114=ELLIPSE('',#6302,1.0823922002924,1.);
#219=SHAPE_REPRESENTATION_RELATIONSHIP('SRR','None',#10173,#229);
#229=ADVANCED_BREP_SHAPE_REPRESENTATION('',(#249),#10125);
#239=STYLED_ITEM('',(#10247),#249);
#249=MANIFOLD_SOLID_BREP('Front_Block_02',#5883);
#281=FACE_BOUND('',#1002,.T.);
#282=FACE_BOUND('',#1003,.T.);
#283=FACE_BOUND('',#1004,.T.);
#284=FACE_BOUND('',#1005,.T.);
#285=FACE_BOUND('',#1006,.T.);
#286=FACE_BOUND('',#1007,.T.);
#287=FACE_BOUND('',#1008,.T.);
#288=FACE_BOUND('',#1009,.T.);
#289=FACE_BOUND('',#1010,.T.);
#290=FACE_BOUND('',#1011,.T.);
#291=FACE_BOUND('',#1024,.T.);
#292=FACE_BOUND('',#1025,.T.);
#293=FACE_BOUND('',#1026,.T.);
#294=FACE_BOUND('',#1027,.T.);
#295=FACE_BOUND('',#1028,.T.);
#296=FACE_BOUND('',#1029,.T.);
#297=FACE_BOUND('',#1030,.T.);
#298=FACE_BOUND('',#1031,.T.);
#299=FACE_BOUND('',#1032,.T.);
#300=FACE_BOUND('',#1033,.T.);
#388=PLANE('',#6283);
#389=PLANE('',#6284);
#390=PLANE('',#6285);
#391=PLANE('',#6286);
#392=PLANE('',#6287);
#393=PLANE('',#6304);
#394=PLANE('',#6305);
#395=PLANE('',#6306);
#396=PLANE('',#6307);
#397=PLANE('',#6308);
#604=FACE_OUTER_BOUND('',#979,.T.);
#605=FACE_OUTER_BOUND('',#980,.T.);
#606=FACE_OUTER_BOUND('',#981,.T.);
#607=FACE_OUTER_BOUND('',#982,.T.);
#608=FACE_OUTER_BOUND('',#983,.T.);
#609=FACE_OUTER_BOUND('',#984,.T.);
#610=FACE_OUTER_BOUND('',#985,.T.);
#611=FACE_OUTER_BOUND('',#986,.T.);
#612=FACE_OUTER_BOUND('',#987,.T.);
#613=FACE_OUTER_BOUND('',#988,.T.);
#614=FACE_OUTER_BOUND('',#989,.T.);
#615=FACE_OUTER_BOUND('',#990,.T.);
#616=FACE_OUTER_BOUND('',#991,.T.);
#617=FACE_OUTER_BOUND('',#992,.T.);
#618=FACE_OUTER_BOUND('',#993,.T.);
#619=FACE_OUTER_BOUND('',#994,.T.);
#620=FACE_OUTER_BOUND('',#995,.T.);
#621=FACE_OUTER_BOUND('',#996,.T.);
#622=FACE_OUTER_BOUND('',#997,.T.);
#623=FACE_OUTER_BOUND('',#998,.T.);
#624=FACE_OUTER_BOUND('',#999,.T.);
#625=FACE_OUTER_BOUND('',#1000,.T.);
#626=FACE_OUTER_BOUND('',#1001,.T.);
#627=FACE_OUTER_BOUND('',#1012,.T.);
#628=FACE_OUTER_BOUND('',#1013,.T.);
#629=FACE_OUTER_BOUND('',#1014,.T.);
#630=FACE_OUTER_BOUND('',#1015,.T.);
#631=FACE_OUTER_BOUND('',#1016,.T.);
#632=FACE_OUTER_BOUND('',#1017,.T.);
#633=FACE_OUTER_BOUND('',#1018,.T.);
#634=FACE_OUTER_BOUND('',#1019,.T.);
#635=FACE_OUTER_BOUND('',#1020,.T.);
#636=FACE_OUTER_BOUND('',#1021,.T.);
#637=FACE_OUTER_BOUND('',#1022,.T.);
#638=FACE_OUTER_BOUND('',#1023,.T.);
#639=FACE_OUTER_BOUND('',#1034,.T.);
#979=EDGE_LOOP('',(#4362,#4363,#4364,#4365));
#980=EDGE_LOOP('',(#4366,#4367,#4368,#4369));
#981=EDGE_LOOP('',(#4370,#4371,#4372,#4373));
#982=EDGE_LOOP('',(#4374,#4375,#4376,#4377));
#983=EDGE_LOOP('',(#4378,#4379,#4380,#4381));
#984=EDGE_LOOP('',(#4382,#4383,#4384,#4385));
#985=EDGE_LOOP('',(#4386,#4387,#4388,#4389));
#986=EDGE_LOOP('',(#4390,#4391,#4392,#4393));
#987=EDGE_LOOP('',(#4394,#4395,#4396,#4397));
#988=EDGE_LOOP('',(#4398,#4399,#4400,#4401));
#989=EDGE_LOOP('',(#4402,#4403,#4404,#4405));
#990=EDGE_LOOP('',(#4406,#4407,#4408,#4409));
#991=EDGE_LOOP('',(#4410,#4411,#4412,#4413));
#992=EDGE_LOOP('',(#4414,#4415,#4416,#4417));
#993=EDGE_LOOP('',(#4418,#4419,#4420,#4421));
#994=EDGE_LOOP('',(#4422,#4423,#4424,#4425));
#995=EDGE_LOOP('',(#4426,#4427,#4428,#4429));
#996=EDGE_LOOP('',(#4430,#4431,#4432,#4433));
#997=EDGE_LOOP('',(#4434,#4435,#4436,#4437));
#998=EDGE_LOOP('',(#4438,#4439,#4440,#4441));
#999=EDGE_LOOP('',(#4442,#4443,#4444,#4445));
#1000=EDGE_LOOP('',(#4446,#4447,#4448,#4449));
#1001=EDGE_LOOP('',(#4450,#4451,#4452,#4453,#4454,#4455,#4456,#4457));
#1002=EDGE_LOOP('',(#4458));
#1003=EDGE_LOOP('',(#4459));
#1004=EDGE_LOOP('',(#4460));
#1005=EDGE_LOOP('',(#4461));
#1006=EDGE_LOOP('',(#4462));
#1007=EDGE_LOOP('',(#4463));
#1008=EDGE_LOOP('',(#4464));
#1009=EDGE_LOOP('',(#4465));
#1010=EDGE_LOOP('',(#4466));
#1011=EDGE_LOOP('',(#4467));
#1012=EDGE_LOOP('',(#4468,#4469,#4470,#4471));
#1013=EDGE_LOOP('',(#4472,#4473,#4474,#4475));
#1014=EDGE_LOOP('',(#4476,#4477,#4478,#4479));
#1015=EDGE_LOOP('',(#4480,#4481,#4482,#4483));
#1016=EDGE_LOOP('',(#4484,#4485,#4486,#4487));
#1017=EDGE_LOOP('',(#4488,#4489,#4490,#4491));
#1018=EDGE_LOOP('',(#4492,#4493,#4494,#4495));
#1019=EDGE_LOOP('',(#4496,#4497,#4498,#4499));
#1020=EDGE_LOOP('',(#4500,#4501,#4502,#4503));
#1021=EDGE_LOOP('',(#4504,#4505,#4506,#4507));
#1022=EDGE_LOOP('',(#4508,#4509,#4510,#4511));
#1023=EDGE_LOOP('',(#4512,#4513,#4514,#4515,#4516,#4517,#4518,#4519));
#1024=EDGE_LOOP('',(#4520));
#1025=EDGE_LOOP('',(#4521));
#1026=EDGE_LOOP('',(#4522));
#1027=EDGE_LOOP('',(#4523));
#1028=EDGE_LOOP('',(#4524));
#1029=EDGE_LOOP('',(#4525));
#1030=EDGE_LOOP('',(#4526));
#1031=EDGE_LOOP('',(#4527));
#1032=EDGE_LOOP('',(#4528));
#1033=EDGE_LOOP('',(#4529));
#1034=EDGE_LOOP('',(#4530,#4531,#4532,#4533));
#1459=LINE('',#9116,#2009);
#1460=LINE('',#9122,#2010);
#1461=LINE('',#9128,#2011);
#1462=LINE('',#9134,#2012);
#1463=LINE('',#9140,#2013);
#1464=LINE('',#9146,#2014);
#1465=LINE('',#9152,#2015);
#1466=LINE('',#9158,#2016);
#1467=LINE('',#9164,#2017);
#1468=LINE('',#9170,#2018);
#1469=LINE('',#9175,#2019);
#1470=LINE('',#9179,#2020);
#1471=LINE('',#9183,#2021);
#1472=LINE('',#9186,#2022);
#1473=LINE('',#9189,#2023);
#1474=LINE('',#9192,#2024);
#1475=LINE('',#9195,#2025);
#1476=LINE('',#9198,#2026);
#1477=LINE('',#9201,#2027);
#1478=LINE('',#9203,#2028);
#1479=LINE('',#9207,#2029);
#1480=LINE('',#9209,#2030);
#1481=LINE('',#9213,#2031);
#1482=LINE('',#9215,#2032);
#1483=LINE('',#9218,#2033);
#1484=LINE('',#9219,#2034);
#1485=LINE('',#9222,#2035);
#1486=LINE('',#9224,#2036);
#1487=LINE('',#9225,#2037);
#1488=LINE('',#9228,#2038);
#1489=LINE('',#9229,#2039);
#1490=LINE('',#9232,#2040);
#1491=LINE('',#9233,#2041);
#1492=LINE('',#9236,#2042);
#1493=LINE('',#9237,#2043);
#1494=LINE('',#9242,#2044);
#1495=LINE('',#9247,#2045);
#1496=LINE('',#9251,#2046);
#1497=LINE('',#9255,#2047);
#1498=LINE('',#9259,#2048);
#1499=LINE('',#9261,#2049);
#1500=LINE('',#9265,#2050);
#1501=LINE('',#9267,#2051);
#1502=LINE('',#9271,#2052);
#1503=LINE('',#9273,#2053);
#1504=LINE('',#9276,#2054);
#1505=LINE('',#9277,#2055);
#1506=LINE('',#9279,#2056);
#1507=LINE('',#9280,#2057);
#1508=LINE('',#9282,#2058);
#2009=VECTOR('',#7325,3.00000000000001);
#2010=VECTOR('',#7332,3.);
#2011=VECTOR('',#7339,2.99999999999999);
#2012=VECTOR('',#7346,3.);
#2013=VECTOR('',#7353,3.);
#2014=VECTOR('',#7360,2.99999999999999);
#2015=VECTOR('',#7367,2.99999999999999);
#2016=VECTOR('',#7374,3.);
#2017=VECTOR('',#7381,3.);
#2018=VECTOR('',#7388,2.99999999999999);
#2019=VECTOR('',#7393,10.);
#2020=VECTOR('',#7396,10.);
#2021=VECTOR('',#7401,10.);
#2022=VECTOR('',#7404,10.);
#2023=VECTOR('',#7407,10.);
#2024=VECTOR('',#7410,10.);
#2025=VECTOR('',#7413,10.);
#2026=VECTOR('',#7416,10.);
#2027=VECTOR('',#7419,10.);
#2028=VECTOR('',#7420,10.);
#2029=VECTOR('',#7425,10.);
#2030=VECTOR('',#7426,10.);
#2031=VECTOR('',#7431,10.);
#2032=VECTOR('',#7432,10.);
#2033=VECTOR('',#7437,10.);
#2034=VECTOR('',#7438,10.);
#2035=VECTOR('',#7441,10.);
#2036=VECTOR('',#7442,10.);
#2037=VECTOR('',#7443,10.);
#2038=VECTOR('',#7446,10.);
#2039=VECTOR('',#7447,10.);
#2040=VECTOR('',#7450,10.);
#2041=VECTOR('',#7451,10.);
#2042=VECTOR('',#7454,10.);
#2043=VECTOR('',#7455,10.);
#2044=VECTOR('',#7460,10.);
#2045=VECTOR('',#7467,10.);
#2046=VECTOR('',#7472,10.);
#2047=VECTOR('',#7477,10.);
#2048=VECTOR('',#7482,10.);
#2049=VECTOR('',#7483,10.);
#2050=VECTOR('',#7488,10.);
#2051=VECTOR('',#7489,10.);
#2052=VECTOR('',#7494,10.);
#2053=VECTOR('',#7495,10.);
#2054=VECTOR('',#7500,10.);
#2055=VECTOR('',#7501,10.);
#2056=VECTOR('',#7504,10.);
#2057=VECTOR('',#7505,10.);
#2058=VECTOR('',#7508,10.);
#2380=CIRCLE('',#6238,3.00000000000001);
#2381=CIRCLE('',#6239,3.00000000000001);
#2382=CIRCLE('',#6241,3.);
#2383=CIRCLE('',#6242,3.);
#2384=CIRCLE('',#6244,2.99999999999999);
#2385=CIRCLE('',#6245,2.99999999999999);
#2386=CIRCLE('',#6247,3.);
#2387=CIRCLE('',#6248,3.);
#2388=CIRCLE('',#6250,3.);
#2389=CIRCLE('',#6251,3.);
#2390=CIRCLE('',#6253,2.99999999999999);
#2391=CIRCLE('',#6254,2.99999999999999);
#2392=CIRCLE('',#6256,2.99999999999999);
#2393=CIRCLE('',#6257,2.99999999999999);
#2394=CIRCLE('',#6259,3.);
#2395=CIRCLE('',#6260,3.);
#2396=CIRCLE('',#6262,3.);
#2397=CIRCLE('',#6263,3.);
#2398=CIRCLE('',#6265,2.99999999999999);
#2399=CIRCLE('',#6266,2.99999999999999);
#2624=VERTEX_POINT('',#9113);
#2625=VERTEX_POINT('',#9115);
#2626=VERTEX_POINT('',#9119);
#2627=VERTEX_POINT('',#9121);
#2628=VERTEX_POINT('',#9125);
#2629=VERTEX_POINT('',#9127);
#2630=VERTEX_POINT('',#9131);
#2631=VERTEX_POINT('',#9133);
#2632=VERTEX_POINT('',#9137);
#2633=VERTEX_POINT('',#9139);
#2634=VERTEX_POINT('',#9143);
#2635=VERTEX_POINT('',#9145);
#2636=VERTEX_POINT('',#9149);
#2637=VERTEX_POINT('',#9151);
#2638=VERTEX_POINT('',#9155);
#2639=VERTEX_POINT('',#9157);
#2640=VERTEX_POINT('',#9161);
#2641=VERTEX_POINT('',#9163);
#2642=VERTEX_POINT('',#9167);
#2643=VERTEX_POINT('',#9169);
#2644=VERTEX_POINT('',#9173);
#2645=VERTEX_POINT('',#9174);
#2646=VERTEX_POINT('',#9176);
#2647=VERTEX_POINT('',#9178);
#2648=VERTEX_POINT('',#9182);
#2649=VERTEX_POINT('',#9184);
#2650=VERTEX_POINT('',#9188);
#2651=VERTEX_POINT('',#9190);
#2652=VERTEX_POINT('',#9194);
#2653=VERTEX_POINT('',#9196);
#2654=VERTEX_POINT('',#9200);
#2655=VERTEX_POINT('',#9202);
#2656=VERTEX_POINT('',#9206);
#2657=VERTEX_POINT('',#9208);
#2658=VERTEX_POINT('',#9212);
#2659=VERTEX_POINT('',#9214);
#2660=VERTEX_POINT('',#9221);
#2661=VERTEX_POINT('',#9223);
#2662=VERTEX_POINT('',#9227);
#2663=VERTEX_POINT('',#9231);
#2664=VERTEX_POINT('',#9235);
#2665=VERTEX_POINT('',#9240);
#2666=VERTEX_POINT('',#9241);
#2667=VERTEX_POINT('',#9246);
#2668=VERTEX_POINT('',#9250);
#2669=VERTEX_POINT('',#9254);
#2670=VERTEX_POINT('',#9258);
#2671=VERTEX_POINT('',#9260);
#2672=VERTEX_POINT('',#9264);
#2673=VERTEX_POINT('',#9266);
#2674=VERTEX_POINT('',#9270);
#2675=VERTEX_POINT('',#9272);
#3233=EDGE_CURVE('',#2624,#2624,#2380,.T.);
#3234=EDGE_CURVE('',#2624,#2625,#1459,.T.);
#3235=EDGE_CURVE('',#2625,#2625,#2381,.T.);
#3236=EDGE_CURVE('',#2626,#2626,#2382,.T.);
#3237=EDGE_CURVE('',#2626,#2627,#1460,.T.);
#3238=EDGE_CURVE('',#2627,#2627,#2383,.T.);
#3239=EDGE_CURVE('',#2628,#2628,#2384,.T.);
#3240=EDGE_CURVE('',#2628,#2629,#1461,.T.);
#3241=EDGE_CURVE('',#2629,#2629,#2385,.T.);
#3242=EDGE_CURVE('',#2630,#2630,#2386,.T.);
#3243=EDGE_CURVE('',#2630,#2631,#1462,.T.);
#3244=EDGE_CURVE('',#2631,#2631,#2387,.T.);
#3245=EDGE_CURVE('',#2632,#2632,#2388,.T.);
#3246=EDGE_CURVE('',#2632,#2633,#1463,.T.);
#3247=EDGE_CURVE('',#2633,#2633,#2389,.T.);
#3248=EDGE_CURVE('',#2634,#2634,#2390,.T.);
#3249=EDGE_CURVE('',#2634,#2635,#1464,.T.);
#3250=EDGE_CURVE('',#2635,#2635,#2391,.T.);
#3251=EDGE_CURVE('',#2636,#2636,#2392,.T.);
#3252=EDGE_CURVE('',#2636,#2637,#1465,.T.);
#3253=EDGE_CURVE('',#2637,#2637,#2393,.T.);
#3254=EDGE_CURVE('',#2638,#2638,#2394,.T.);
#3255=EDGE_CURVE('',#2638,#2639,#1466,.T.);
#3256=EDGE_CURVE('',#2639,#2639,#2395,.T.);
#3257=EDGE_CURVE('',#2640,#2640,#2396,.T.);
#3258=EDGE_CURVE('',#2640,#2641,#1467,.T.);
#3259=EDGE_CURVE('',#2641,#2641,#2397,.T.);
#3260=EDGE_CURVE('',#2642,#2642,#2398,.T.);
#3261=EDGE_CURVE('',#2642,#2643,#1468,.T.);
#3262=EDGE_CURVE('',#2643,#2643,#2399,.T.);
#3263=EDGE_CURVE('',#2644,#2645,#1469,.T.);
#3264=EDGE_CURVE('',#2645,#2646,#99,.T.);
#3265=EDGE_CURVE('',#2646,#2647,#1470,.T.);
#3266=EDGE_CURVE('',#2647,#2644,#100,.T.);
#3267=EDGE_CURVE('',#2645,#2648,#1471,.T.);
#3268=EDGE_CURVE('',#2648,#2649,#101,.T.);
#3269=EDGE_CURVE('',#2649,#2646,#1472,.T.);
#3270=EDGE_CURVE('',#2648,#2650,#1473,.T.);
#3271=EDGE_CURVE('',#2650,#2651,#102,.T.);
#3272=EDGE_CURVE('',#2651,#2649,#1474,.T.);
#3273=EDGE_CURVE('',#2650,#2652,#1475,.T.);
#3274=EDGE_CURVE('',#2652,#2653,#103,.T.);
#3275=EDGE_CURVE('',#2653,#2651,#1476,.T.);
#3276=EDGE_CURVE('',#2654,#2653,#1477,.T.);
#3277=EDGE_CURVE('',#2652,#2655,#1478,.T.);
#3278=EDGE_CURVE('',#2655,#2654,#104,.T.);
#3279=EDGE_CURVE('',#2656,#2654,#1479,.T.);
#3280=EDGE_CURVE('',#2655,#2657,#1480,.T.);
#3281=EDGE_CURVE('',#2657,#2656,#105,.T.);
#3282=EDGE_CURVE('',#2658,#2656,#1481,.T.);
#3283=EDGE_CURVE('',#2657,#2659,#1482,.T.);
#3284=EDGE_CURVE('',#2659,#2658,#106,.T.);
#3285=EDGE_CURVE('',#2659,#2644,#1483,.T.);
#3286=EDGE_CURVE('',#2647,#2658,#1484,.T.);
#3287=EDGE_CURVE('',#2650,#2660,#1485,.T.);
#3288=EDGE_CURVE('',#2661,#2660,#1486,.T.);
#3289=EDGE_CURVE('',#2661,#2652,#1487,.T.);
#3290=EDGE_CURVE('',#2662,#2648,#1488,.T.);
#3291=EDGE_CURVE('',#2660,#2662,#1489,.T.);
#3292=EDGE_CURVE('',#2645,#2663,#1490,.T.);
#3293=EDGE_CURVE('',#2662,#2663,#1491,.T.);
#3294=EDGE_CURVE('',#2664,#2644,#1492,.T.);
#3295=EDGE_CURVE('',#2663,#2664,#1493,.T.);
#3296=EDGE_CURVE('',#2665,#2666,#1494,.T.);
#3297=EDGE_CURVE('',#2666,#2663,#107,.T.);
#3298=EDGE_CURVE('',#2665,#2664,#108,.T.);
#3299=EDGE_CURVE('',#2666,#2667,#1495,.T.);
#3300=EDGE_CURVE('',#2667,#2662,#109,.T.);
#3301=EDGE_CURVE('',#2667,#2668,#1496,.T.);
#3302=EDGE_CURVE('',#2668,#2660,#110,.T.);
#3303=EDGE_CURVE('',#2668,#2669,#1497,.T.);
#3304=EDGE_CURVE('',#2669,#2661,#111,.T.);
#3305=EDGE_CURVE('',#2670,#2661,#1498,.T.);
#3306=EDGE_CURVE('',#2669,#2671,#1499,.T.);
#3307=EDGE_CURVE('',#2671,#2670,#112,.T.);
#3308=EDGE_CURVE('',#2672,#2670,#1500,.T.);
#3309=EDGE_CURVE('',#2671,#2673,#1501,.T.);
#3310=EDGE_CURVE('',#2673,#2672,#113,.T.);
#3311=EDGE_CURVE('',#2674,#2672,#1502,.T.);
#3312=EDGE_CURVE('',#2673,#2675,#1503,.T.);
#3313=EDGE_CURVE('',#2675,#2674,#114,.T.);
#3314=EDGE_CURVE('',#2664,#2674,#1504,.T.);
#3315=EDGE_CURVE('',#2675,#2665,#1505,.T.);
#3316=EDGE_CURVE('',#2655,#2670,#1506,.T.);
#3317=EDGE_CURVE('',#2672,#2657,#1507,.T.);
#3318=EDGE_CURVE('',#2659,#2674,#1508,.T.);
#4362=ORIENTED_EDGE('',*,*,#3233,.F.);
#4363=ORIENTED_EDGE('',*,*,#3234,.T.);
#4364=ORIENTED_EDGE('',*,*,#3235,.F.);
#4365=ORIENTED_EDGE('',*,*,#3234,.F.);
#4366=ORIENTED_EDGE('',*,*,#3236,.F.);
#4367=ORIENTED_EDGE('',*,*,#3237,.T.);
#4368=ORIENTED_EDGE('',*,*,#3238,.F.);
#4369=ORIENTED_EDGE('',*,*,#3237,.F.);
#4370=ORIENTED_EDGE('',*,*,#3239,.F.);
#4371=ORIENTED_EDGE('',*,*,#3240,.T.);
#4372=ORIENTED_EDGE('',*,*,#3241,.F.);
#4373=ORIENTED_EDGE('',*,*,#3240,.F.);
#4374=ORIENTED_EDGE('',*,*,#3242,.F.);
#4375=ORIENTED_EDGE('',*,*,#3243,.T.);
#4376=ORIENTED_EDGE('',*,*,#3244,.F.);
#4377=ORIENTED_EDGE('',*,*,#3243,.F.);
#4378=ORIENTED_EDGE('',*,*,#3245,.F.);
#4379=ORIENTED_EDGE('',*,*,#3246,.T.);
#4380=ORIENTED_EDGE('',*,*,#3247,.F.);
#4381=ORIENTED_EDGE('',*,*,#3246,.F.);
#4382=ORIENTED_EDGE('',*,*,#3248,.F.);
#4383=ORIENTED_EDGE('',*,*,#3249,.T.);
#4384=ORIENTED_EDGE('',*,*,#3250,.F.);
#4385=ORIENTED_EDGE('',*,*,#3249,.F.);
#4386=ORIENTED_EDGE('',*,*,#3251,.F.);
#4387=ORIENTED_EDGE('',*,*,#3252,.T.);
#4388=ORIENTED_EDGE('',*,*,#3253,.F.);
#4389=ORIENTED_EDGE('',*,*,#3252,.F.);
#4390=ORIENTED_EDGE('',*,*,#3254,.F.);
#4391=ORIENTED_EDGE('',*,*,#3255,.T.);
#4392=ORIENTED_EDGE('',*,*,#3256,.F.);
#4393=ORIENTED_EDGE('',*,*,#3255,.F.);
#4394=ORIENTED_EDGE('',*,*,#3257,.F.);
#4395=ORIENTED_EDGE('',*,*,#3258,.T.);
#4396=ORIENTED_EDGE('',*,*,#3259,.F.);
#4397=ORIENTED_EDGE('',*,*,#3258,.F.);
#4398=ORIENTED_EDGE('',*,*,#3260,.F.);
#4399=ORIENTED_EDGE('',*,*,#3261,.T.);
#4400=ORIENTED_EDGE('',*,*,#3262,.F.);
#4401=ORIENTED_EDGE('',*,*,#3261,.F.);
#4402=ORIENTED_EDGE('',*,*,#3263,.T.);
#4403=ORIENTED_EDGE('',*,*,#3264,.T.);
#4404=ORIENTED_EDGE('',*,*,#3265,.T.);
#4405=ORIENTED_EDGE('',*,*,#3266,.T.);
#4406=ORIENTED_EDGE('',*,*,#3267,.T.);
#4407=ORIENTED_EDGE('',*,*,#3268,.T.);
#4408=ORIENTED_EDGE('',*,*,#3269,.T.);
#4409=ORIENTED_EDGE('',*,*,#3264,.F.);
#4410=ORIENTED_EDGE('',*,*,#3270,.T.);
#4411=ORIENTED_EDGE('',*,*,#3271,.T.);
#4412=ORIENTED_EDGE('',*,*,#3272,.T.);
#4413=ORIENTED_EDGE('',*,*,#3268,.F.);
#4414=ORIENTED_EDGE('',*,*,#3273,.T.);
#4415=ORIENTED_EDGE('',*,*,#3274,.T.);
#4416=ORIENTED_EDGE('',*,*,#3275,.T.);
#4417=ORIENTED_EDGE('',*,*,#3271,.F.);
#4418=ORIENTED_EDGE('',*,*,#3276,.T.);
#4419=ORIENTED_EDGE('',*,*,#3274,.F.);
#4420=ORIENTED_EDGE('',*,*,#3277,.T.);
#4421=ORIENTED_EDGE('',*,*,#3278,.T.);
#4422=ORIENTED_EDGE('',*,*,#3279,.T.);
#4423=ORIENTED_EDGE('',*,*,#3278,.F.);
#4424=ORIENTED_EDGE('',*,*,#3280,.T.);
#4425=ORIENTED_EDGE('',*,*,#3281,.T.);
#4426=ORIENTED_EDGE('',*,*,#3282,.T.);
#4427=ORIENTED_EDGE('',*,*,#3281,.F.);
#4428=ORIENTED_EDGE('',*,*,#3283,.T.);
#4429=ORIENTED_EDGE('',*,*,#3284,.T.);
#4430=ORIENTED_EDGE('',*,*,#3285,.T.);
#4431=ORIENTED_EDGE('',*,*,#3266,.F.);
#4432=ORIENTED_EDGE('',*,*,#3286,.T.);
#4433=ORIENTED_EDGE('',*,*,#3284,.F.);
#4434=ORIENTED_EDGE('',*,*,#3273,.F.);
#4435=ORIENTED_EDGE('',*,*,#3287,.T.);
#4436=ORIENTED_EDGE('',*,*,#3288,.F.);
#4437=ORIENTED_EDGE('',*,*,#3289,.T.);
#4438=ORIENTED_EDGE('',*,*,#3270,.F.);
#4439=ORIENTED_EDGE('',*,*,#3290,.F.);
#4440=ORIENTED_EDGE('',*,*,#3291,.F.);
#4441=ORIENTED_EDGE('',*,*,#3287,.F.);
#4442=ORIENTED_EDGE('',*,*,#3267,.F.);
#4443=ORIENTED_EDGE('',*,*,#3292,.T.);
#4444=ORIENTED_EDGE('',*,*,#3293,.F.);
#4445=ORIENTED_EDGE('',*,*,#3290,.T.);
#4446=ORIENTED_EDGE('',*,*,#3263,.F.);
#4447=ORIENTED_EDGE('',*,*,#3294,.F.);
#4448=ORIENTED_EDGE('',*,*,#3295,.F.);
#4449=ORIENTED_EDGE('',*,*,#3292,.F.);
#4450=ORIENTED_EDGE('',*,*,#3265,.F.);
#4451=ORIENTED_EDGE('',*,*,#3269,.F.);
#4452=ORIENTED_EDGE('',*,*,#3272,.F.);
#4453=ORIENTED_EDGE('',*,*,#3275,.F.);
#4454=ORIENTED_EDGE('',*,*,#3276,.F.);
#4455=ORIENTED_EDGE('',*,*,#3279,.F.);
#4456=ORIENTED_EDGE('',*,*,#3282,.F.);
#4457=ORIENTED_EDGE('',*,*,#3286,.F.);
#4458=ORIENTED_EDGE('',*,*,#3241,.T.);
#4459=ORIENTED_EDGE('',*,*,#3244,.T.);
#4460=ORIENTED_EDGE('',*,*,#3247,.T.);
#4461=ORIENTED_EDGE('',*,*,#3250,.T.);
#4462=ORIENTED_EDGE('',*,*,#3253,.T.);
#4463=ORIENTED_EDGE('',*,*,#3256,.T.);
#4464=ORIENTED_EDGE('',*,*,#3259,.T.);
#4465=ORIENTED_EDGE('',*,*,#3262,.T.);
#4466=ORIENTED_EDGE('',*,*,#3238,.T.);
#4467=ORIENTED_EDGE('',*,*,#3235,.T.);
#4468=ORIENTED_EDGE('',*,*,#3296,.T.);
#4469=ORIENTED_EDGE('',*,*,#3297,.T.);
#4470=ORIENTED_EDGE('',*,*,#3295,.T.);
#4471=ORIENTED_EDGE('',*,*,#3298,.F.);
#4472=ORIENTED_EDGE('',*,*,#3299,.T.);
#4473=ORIENTED_EDGE('',*,*,#3300,.T.);
#4474=ORIENTED_EDGE('',*,*,#3293,.T.);
#4475=ORIENTED_EDGE('',*,*,#3297,.F.);
#4476=ORIENTED_EDGE('',*,*,#3301,.T.);
#4477=ORIENTED_EDGE('',*,*,#3302,.T.);
#4478=ORIENTED_EDGE('',*,*,#3291,.T.);
#4479=ORIENTED_EDGE('',*,*,#3300,.F.);
#4480=ORIENTED_EDGE('',*,*,#3288,.T.);
#4481=ORIENTED_EDGE('',*,*,#3302,.F.);
#4482=ORIENTED_EDGE('',*,*,#3303,.T.);
#4483=ORIENTED_EDGE('',*,*,#3304,.T.);
#4484=ORIENTED_EDGE('',*,*,#3305,.T.);
#4485=ORIENTED_EDGE('',*,*,#3304,.F.);
#4486=ORIENTED_EDGE('',*,*,#3306,.T.);
#4487=ORIENTED_EDGE('',*,*,#3307,.T.);
#4488=ORIENTED_EDGE('',*,*,#3308,.T.);
#4489=ORIENTED_EDGE('',*,*,#3307,.F.);
#4490=ORIENTED_EDGE('',*,*,#3309,.T.);
#4491=ORIENTED_EDGE('',*,*,#3310,.T.);
#4492=ORIENTED_EDGE('',*,*,#3311,.T.);
#4493=ORIENTED_EDGE('',*,*,#3310,.F.);
#4494=ORIENTED_EDGE('',*,*,#3312,.T.);
#4495=ORIENTED_EDGE('',*,*,#3313,.T.);
#4496=ORIENTED_EDGE('',*,*,#3314,.T.);
#4497=ORIENTED_EDGE('',*,*,#3313,.F.);
#4498=ORIENTED_EDGE('',*,*,#3315,.T.);
#4499=ORIENTED_EDGE('',*,*,#3298,.T.);
#4500=ORIENTED_EDGE('',*,*,#3280,.F.);
#4501=ORIENTED_EDGE('',*,*,#3316,.T.);
#4502=ORIENTED_EDGE('',*,*,#3308,.F.);
#4503=ORIENTED_EDGE('',*,*,#3317,.T.);
#4504=ORIENTED_EDGE('',*,*,#3283,.F.);
#4505=ORIENTED_EDGE('',*,*,#3317,.F.);
#4506=ORIENTED_EDGE('',*,*,#3311,.F.);
#4507=ORIENTED_EDGE('',*,*,#3318,.F.);
#4508=ORIENTED_EDGE('',*,*,#3285,.F.);
#4509=ORIENTED_EDGE('',*,*,#3318,.T.);
#4510=ORIENTED_EDGE('',*,*,#3314,.F.);
#4511=ORIENTED_EDGE('',*,*,#3294,.T.);
#4512=ORIENTED_EDGE('',*,*,#3296,.F.);
#4513=ORIENTED_EDGE('',*,*,#3315,.F.);
#4514=ORIENTED_EDGE('',*,*,#3312,.F.);
#4515=ORIENTED_EDGE('',*,*,#3309,.F.);
#4516=ORIENTED_EDGE('',*,*,#3306,.F.);
#4517=ORIENTED_EDGE('',*,*,#3303,.F.);
#4518=ORIENTED_EDGE('',*,*,#3301,.F.);
#4519=ORIENTED_EDGE('',*,*,#3299,.F.);
#4520=ORIENTED_EDGE('',*,*,#3239,.T.);
#4521=ORIENTED_EDGE('',*,*,#3242,.T.);
#4522=ORIENTED_EDGE('',*,*,#3245,.T.);
#4523=ORIENTED_EDGE('',*,*,#3248,.T.);
#4524=ORIENTED_EDGE('',*,*,#3251,.T.);
#4525=ORIENTED_EDGE('',*,*,#3254,.T.);
#4526=ORIENTED_EDGE('',*,*,#3257,.T.);
#4527=ORIENTED_EDGE('',*,*,#3260,.T.);
#4528=ORIENTED_EDGE('',*,*,#3236,.T.);
#4529=ORIENTED_EDGE('',*,*,#3233,.T.);
#4530=ORIENTED_EDGE('',*,*,#3277,.F.);
#4531=ORIENTED_EDGE('',*,*,#3289,.F.);
#4532=ORIENTED_EDGE('',*,*,#3305,.F.);
#4533=ORIENTED_EDGE('',*,*,#3316,.F.);
#5397=CYLINDRICAL_SURFACE('',#6237,3.00000000000001);
#5398=CYLINDRICAL_SURFACE('',#6240,3.);
#5399=CYLINDRICAL_SURFACE('',#6243,2.99999999999999);
#5400=CYLINDRICAL_SURFACE('',#6246,3.);
#5401=CYLINDRICAL_SURFACE('',#6249,3.);
#5402=CYLINDRICAL_SURFACE('',#6252,2.99999999999999);
#5403=CYLINDRICAL_SURFACE('',#6255,2.99999999999999);
#5404=CYLINDRICAL_SURFACE('',#6258,3.);
#5405=CYLINDRICAL_SURFACE('',#6261,3.);
#5406=CYLINDRICAL_SURFACE('',#6264,2.99999999999999);
#5407=CYLINDRICAL_SURFACE('',#6267,1.);
#5408=CYLINDRICAL_SURFACE('',#6270,1.);
#5409=CYLINDRICAL_SURFACE('',#6272,1.);
#5410=CYLINDRICAL_SURFACE('',#6274,1.);
#5411=CYLINDRICAL_SURFACE('',#6276,1.);
#5412=CYLINDRICAL_SURFACE('',#6278,1.);
#5413=CYLINDRICAL_SURFACE('',#6280,1.);
#5414=CYLINDRICAL_SURFACE('',#6282,1.);
#5415=CYLINDRICAL_SURFACE('',#6288,1.);
#5416=CYLINDRICAL_SURFACE('',#6291,1.);
#5417=CYLINDRICAL_SURFACE('',#6293,1.);
#5418=CYLINDRICAL_SURFACE('',#6295,1.);
#5419=CYLINDRICAL_SURFACE('',#6297,1.);
#5420=CYLINDRICAL_SURFACE('',#6299,1.);
#5421=CYLINDRICAL_SURFACE('',#6301,1.);
#5422=CYLINDRICAL_SURFACE('',#6303,1.);
#5667=ADVANCED_FACE('',(#604),#5397,.F.);
#5668=ADVANCED_FACE('',(#605),#5398,.F.);
#5669=ADVANCED_FACE('',(#606),#5399,.F.);
#5670=ADVANCED_FACE('',(#607),#5400,.F.);
#5671=ADVANCED_FACE('',(#608),#5401,.F.);
#5672=ADVANCED_FACE('',(#609),#5402,.F.);
#5673=ADVANCED_FACE('',(#610),#5403,.F.);
#5674=ADVANCED_FACE('',(#611),#5404,.F.);
#5675=ADVANCED_FACE('',(#612),#5405,.F.);
#5676=ADVANCED_FACE('',(#613),#5406,.F.);
#5677=ADVANCED_FACE('',(#614),#5407,.T.);
#5678=ADVANCED_FACE('',(#615),#5408,.T.);
#5679=ADVANCED_FACE('',(#616),#5409,.T.);
#5680=ADVANCED_FACE('',(#617),#5410,.T.);
#5681=ADVANCED_FACE('',(#618),#5411,.T.);
#5682=ADVANCED_FACE('',(#619),#5412,.T.);
#5683=ADVANCED_FACE('',(#620),#5413,.T.);
#5684=ADVANCED_FACE('',(#621),#5414,.T.);
#5685=ADVANCED_FACE('',(#622),#388,.T.);
#5686=ADVANCED_FACE('',(#623),#389,.T.);
#5687=ADVANCED_FACE('',(#624),#390,.T.);
#5688=ADVANCED_FACE('',(#625),#391,.T.);
#5689=ADVANCED_FACE('',(#626,#281,#282,#283,#284,#285,#286,#287,#288,#289,
#290),#392,.F.);
#5690=ADVANCED_FACE('',(#627),#5415,.T.);
#5691=ADVANCED_FACE('',(#628),#5416,.T.);
#5692=ADVANCED_FACE('',(#629),#5417,.T.);
#5693=ADVANCED_FACE('',(#630),#5418,.T.);
#5694=ADVANCED_FACE('',(#631),#5419,.T.);
#5695=ADVANCED_FACE('',(#632),#5420,.T.);
#5696=ADVANCED_FACE('',(#633),#5421,.T.);
#5697=ADVANCED_FACE('',(#634),#5422,.T.);
#5698=ADVANCED_FACE('',(#635),#393,.T.);
#5699=ADVANCED_FACE('',(#636),#394,.T.);
#5700=ADVANCED_FACE('',(#637),#395,.T.);
#5701=ADVANCED_FACE('',(#638,#291,#292,#293,#294,#295,#296,#297,#298,#299,
#300),#396,.T.);
#5702=ADVANCED_FACE('',(#639),#397,.T.);
#5883=CLOSED_SHELL('',(#5667,#5668,#5669,#5670,#5671,#5672,#5673,#5674,
#5675,#5676,#5677,#5678,#5679,#5680,#5681,#5682,#5683,#5684,#5685,#5686,
#5687,#5688,#5689,#5690,#5691,#5692,#5693,#5694,#5695,#5696,#5697,#5698,
#5699,#5700,#5701,#5702));
#6236=AXIS2_PLACEMENT_3D('',#9111,#7319,#7320);
#6237=AXIS2_PLACEMENT_3D('',#9112,#7321,#7322);
#6238=AXIS2_PLACEMENT_3D('',#9114,#7323,#7324);
#6239=AXIS2_PLACEMENT_3D('',#9117,#7326,#7327);
#6240=AXIS2_PLACEMENT_3D('',#9118,#7328,#7329);
#6241=AXIS2_PLACEMENT_3D('',#9120,#7330,#7331);
#6242=AXIS2_PLACEMENT_3D('',#9123,#7333,#7334);
#6243=AXIS2_PLACEMENT_3D('',#9124,#7335,#7336);
#6244=AXIS2_PLACEMENT_3D('',#9126,#7337,#7338);
#6245=AXIS2_PLACEMENT_3D('',#9129,#7340,#7341);
#6246=AXIS2_PLACEMENT_3D('',#9130,#7342,#7343);
#6247=AXIS2_PLACEMENT_3D('',#9132,#7344,#7345);
#6248=AXIS2_PLACEMENT_3D('',#9135,#7347,#7348);
#6249=AXIS2_PLACEMENT_3D('',#9136,#7349,#7350);
#6250=AXIS2_PLACEMENT_3D('',#9138,#7351,#7352);
#6251=AXIS2_PLACEMENT_3D('',#9141,#7354,#7355);
#6252=AXIS2_PLACEMENT_3D('',#9142,#7356,#7357);
#6253=AXIS2_PLACEMENT_3D('',#9144,#7358,#7359);
#6254=AXIS2_PLACEMENT_3D('',#9147,#7361,#7362);
#6255=AXIS2_PLACEMENT_3D('',#9148,#7363,#7364);
#6256=AXIS2_PLACEMENT_3D('',#9150,#7365,#7366);
#6257=AXIS2_PLACEMENT_3D('',#9153,#7368,#7369);
#6258=AXIS2_PLACEMENT_3D('',#9154,#7370,#7371);
#6259=AXIS2_PLACEMENT_3D('',#9156,#7372,#7373);
#6260=AXIS2_PLACEMENT_3D('',#9159,#7375,#7376);
#6261=AXIS2_PLACEMENT_3D('',#9160,#7377,#7378);
#6262=AXIS2_PLACEMENT_3D('',#9162,#7379,#7380);
#6263=AXIS2_PLACEMENT_3D('',#9165,#7382,#7383);
#6264=AXIS2_PLACEMENT_3D('',#9166,#7384,#7385);
#6265=AXIS2_PLACEMENT_3D('',#9168,#7386,#7387);
#6266=AXIS2_PLACEMENT_3D('',#9171,#7389,#7390);
#6267=AXIS2_PLACEMENT_3D('',#9172,#7391,#7392);
#6268=AXIS2_PLACEMENT_3D('',#9177,#7394,#7395);
#6269=AXIS2_PLACEMENT_3D('',#9180,#7397,#7398);
#6270=AXIS2_PLACEMENT_3D('',#9181,#7399,#7400);
#6271=AXIS2_PLACEMENT_3D('',#9185,#7402,#7403);
#6272=AXIS2_PLACEMENT_3D('',#9187,#7405,#7406);
#6273=AXIS2_PLACEMENT_3D('',#9191,#7408,#7409);
#6274=AXIS2_PLACEMENT_3D('',#9193,#7411,#7412);
#6275=AXIS2_PLACEMENT_3D('',#9197,#7414,#7415);
#6276=AXIS2_PLACEMENT_3D('',#9199,#7417,#7418);
#6277=AXIS2_PLACEMENT_3D('',#9204,#7421,#7422);
#6278=AXIS2_PLACEMENT_3D('',#9205,#7423,#7424);
#6279=AXIS2_PLACEMENT_3D('',#9210,#7427,#7428);
#6280=AXIS2_PLACEMENT_3D('',#9211,#7429,#7430);
#6281=AXIS2_PLACEMENT_3D('',#9216,#7433,#7434);
#6282=AXIS2_PLACEMENT_3D('',#9217,#7435,#7436);
#6283=AXIS2_PLACEMENT_3D('',#9220,#7439,#7440);
#6284=AXIS2_PLACEMENT_3D('',#9226,#7444,#7445);
#6285=AXIS2_PLACEMENT_3D('',#9230,#7448,#7449);
#6286=AXIS2_PLACEMENT_3D('',#9234,#7452,#7453);
#6287=AXIS2_PLACEMENT_3D('',#9238,#7456,#7457);
#6288=AXIS2_PLACEMENT_3D('',#9239,#7458,#7459);
#6289=AXIS2_PLACEMENT_3D('',#9243,#7461,#7462);
#6290=AXIS2_PLACEMENT_3D('',#9244,#7463,#7464);
#6291=AXIS2_PLACEMENT_3D('',#9245,#7465,#7466);
#6292=AXIS2_PLACEMENT_3D('',#9248,#7468,#7469);
#6293=AXIS2_PLACEMENT_3D('',#9249,#7470,#7471);
#6294=AXIS2_PLACEMENT_3D('',#9252,#7473,#7474);
#6295=AXIS2_PLACEMENT_3D('',#9253,#7475,#7476);
#6296=AXIS2_PLACEMENT_3D('',#9256,#7478,#7479);
#6297=AXIS2_PLACEMENT_3D('',#9257,#7480,#7481);
#6298=AXIS2_PLACEMENT_3D('',#9262,#7484,#7485);
#6299=AXIS2_PLACEMENT_3D('',#9263,#7486,#7487);
#6300=AXIS2_PLACEMENT_3D('',#9268,#7490,#7491);
#6301=AXIS2_PLACEMENT_3D('',#9269,#7492,#7493);
#6302=AXIS2_PLACEMENT_3D('',#9274,#7496,#7497);
#6303=AXIS2_PLACEMENT_3D('',#9275,#7498,#7499);
#6304=AXIS2_PLACEMENT_3D('',#9278,#7502,#7503);
#6305=AXIS2_PLACEMENT_3D('',#9281,#7506,#7507);
#6306=AXIS2_PLACEMENT_3D('',#9283,#7509,#7510);
#6307=AXIS2_PLACEMENT_3D('',#9284,#7511,#7512);
#6308=AXIS2_PLACEMENT_3D('',#9285,#7513,#7514);
#7319=DIRECTION('axis',(0.,0.,1.));
#7320=DIRECTION('refdir',(1.,0.,0.));
#7321=DIRECTION('center_axis',(0.,1.,0.));
#7322=DIRECTION('ref_axis',(1.,0.,0.));
#7323=DIRECTION('center_axis',(0.,1.,0.));
#7324=DIRECTION('ref_axis',(1.,0.,0.));
#7325=DIRECTION('',(0.,1.,0.));
#7326=DIRECTION('center_axis',(0.,-1.,0.));
#7327=DIRECTION('ref_axis',(1.,0.,0.));
#7328=DIRECTION('center_axis',(0.,1.,0.));
#7329=DIRECTION('ref_axis',(1.,0.,0.));
#7330=DIRECTION('center_axis',(0.,1.,0.));
#7331=DIRECTION('ref_axis',(1.,0.,0.));
#7332=DIRECTION('',(0.,1.,0.));
#7333=DIRECTION('center_axis',(0.,-1.,0.));
#7334=DIRECTION('ref_axis',(1.,0.,0.));
#7335=DIRECTION('center_axis',(0.,1.,0.));
#7336=DIRECTION('ref_axis',(1.,0.,0.));
#7337=DIRECTION('center_axis',(0.,1.,0.));
#7338=DIRECTION('ref_axis',(1.,0.,0.));
#7339=DIRECTION('',(0.,1.,0.));
#7340=DIRECTION('center_axis',(0.,-1.,0.));
#7341=DIRECTION('ref_axis',(1.,0.,0.));
#7342=DIRECTION('center_axis',(0.,1.,0.));
#7343=DIRECTION('ref_axis',(1.,0.,0.));
#7344=DIRECTION('center_axis',(0.,1.,0.));
#7345=DIRECTION('ref_axis',(1.,0.,0.));
#7346=DIRECTION('',(0.,1.,0.));
#7347=DIRECTION('center_axis',(0.,-1.,0.));
#7348=DIRECTION('ref_axis',(1.,0.,0.));
#7349=DIRECTION('center_axis',(0.,1.,0.));
#7350=DIRECTION('ref_axis',(1.,0.,0.));
#7351=DIRECTION('center_axis',(0.,1.,0.));
#7352=DIRECTION('ref_axis',(1.,0.,0.));
#7353=DIRECTION('',(0.,1.,0.));
#7354=DIRECTION('center_axis',(0.,-1.,0.));
#7355=DIRECTION('ref_axis',(1.,0.,0.));
#7356=DIRECTION('center_axis',(0.,1.,0.));
#7357=DIRECTION('ref_axis',(1.,0.,0.));
#7358=DIRECTION('center_axis',(0.,1.,0.));
#7359=DIRECTION('ref_axis',(1.,0.,0.));
#7360=DIRECTION('',(0.,1.,0.));
#7361=DIRECTION('center_axis',(0.,-1.,0.));
#7362=DIRECTION('ref_axis',(1.,0.,0.));
#7363=DIRECTION('center_axis',(0.,1.,0.));
#7364=DIRECTION('ref_axis',(1.,0.,0.));
#7365=DIRECTION('center_axis',(0.,1.,0.));
#7366=DIRECTION('ref_axis',(1.,0.,0.));
#7367=DIRECTION('',(0.,1.,0.));
#7368=DIRECTION('center_axis',(0.,-1.,0.));
#7369=DIRECTION('ref_axis',(1.,0.,0.));
#7370=DIRECTION('center_axis',(0.,1.,0.));
#7371=DIRECTION('ref_axis',(1.,0.,0.));
#7372=DIRECTION('center_axis',(0.,1.,0.));
#7373=DIRECTION('ref_axis',(1.,0.,0.));
#7374=DIRECTION('',(0.,1.,0.));
#7375=DIRECTION('center_axis',(0.,-1.,0.));
#7376=DIRECTION('ref_axis',(1.,0.,0.));
#7377=DIRECTION('center_axis',(0.,1.,0.));
#7378=DIRECTION('ref_axis',(1.,0.,0.));
#7379=DIRECTION('center_axis',(0.,1.,0.));
#7380=DIRECTION('ref_axis',(1.,0.,0.));
#7381=DIRECTION('',(0.,1.,0.));
#7382=DIRECTION('center_axis',(0.,-1.,0.));
#7383=DIRECTION('ref_axis',(1.,0.,0.));
#7384=DIRECTION('center_axis',(0.,1.,0.));
#7385=DIRECTION('ref_axis',(1.,0.,0.));
#7386=DIRECTION('center_axis',(0.,1.,0.));
#7387=DIRECTION('ref_axis',(1.,0.,0.));
#7388=DIRECTION('',(0.,1.,0.));
#7389=DIRECTION('center_axis',(0.,-1.,0.));
#7390=DIRECTION('ref_axis',(1.,0.,0.));
#7391=DIRECTION('center_axis',(0.,0.,1.));
#7392=DIRECTION('ref_axis',(0.707106781186548,0.707106781186548,0.));
#7393=DIRECTION('',(0.,0.,-1.));
#7394=DIRECTION('center_axis',(0.382683432365099,-8.20569863179165E-15,
0.923879532511283));
#7395=DIRECTION('ref_axis',(0.923879532511283,-1.98103089256172E-14,-0.382683432365098));
#7396=DIRECTION('',(0.,0.,1.));
#7397=DIRECTION('center_axis',(0.382683432365092,-1.98103089256178E-14,
-0.923879532511286));
#7398=DIRECTION('ref_axis',(-0.923879532511286,4.78263164830271E-14,-0.382683432365092));
#7399=DIRECTION('center_axis',(0.707106781186548,0.,0.707106781186548));
#7400=DIRECTION('ref_axis',(0.499999999999999,0.707106781186545,-0.500000000000005));
#7401=DIRECTION('',(-0.707106781186548,0.,-0.707106781186548));
#7402=DIRECTION('center_axis',(0.923879532511283,0.,0.382683432365099));
#7403=DIRECTION('ref_axis',(0.382683432365099,0.,-0.923879532511283));
#7404=DIRECTION('',(0.707106781186548,0.,0.707106781186548));
#7405=DIRECTION('center_axis',(1.,0.,0.));
#7406=DIRECTION('ref_axis',(0.,0.707106781186548,-0.707106781186548));
#7407=DIRECTION('',(-1.,0.,0.));
#7408=DIRECTION('center_axis',(0.923879532511286,1.69945583101724E-15,-0.382683432365092));
#7409=DIRECTION('ref_axis',(-0.382683432365092,4.10284931589584E-15,-0.923879532511286));
#7410=DIRECTION('',(1.,0.,0.));
#7411=DIRECTION('center_axis',(0.707106781186548,0.,-0.707106781186548));
#7412=DIRECTION('ref_axis',(-0.5,0.707106781186547,-0.5));
#7413=DIRECTION('',(-0.707106781186548,0.,0.707106781186548));
#7414=DIRECTION('center_axis',(0.382683432365092,0.,-0.923879532511286));
#7415=DIRECTION('ref_axis',(-0.923879532511286,0.,-0.382683432365091));
#7416=DIRECTION('',(0.707106781186548,0.,-0.707106781186548));
#7417=DIRECTION('center_axis',(0.,0.,-1.));
#7418=DIRECTION('ref_axis',(-0.707106781186548,0.707106781186548,0.));
#7419=DIRECTION('',(0.,0.,-1.));
#7420=DIRECTION('',(0.,0.,1.));
#7421=DIRECTION('center_axis',(-0.382683432365106,0.,-0.92387953251128));
#7422=DIRECTION('ref_axis',(-0.92387953251128,0.,0.382683432365106));
#7423=DIRECTION('center_axis',(-0.707106781186548,0.,-0.707106781186548));
#7424=DIRECTION('ref_axis',(-0.5,0.707106781186547,0.5));
#7425=DIRECTION('',(-0.707106781186548,0.,-0.707106781186548));
#7426=DIRECTION('',(0.707106781186548,0.,0.707106781186548));
#7427=DIRECTION('center_axis',(-0.923879532511291,0.,-0.382683432365079));
#7428=DIRECTION('ref_axis',(-0.382683432365079,0.,0.923879532511291));
#7429=DIRECTION('center_axis',(-1.,0.,0.));
#7430=DIRECTION('ref_axis',(0.,0.707106781186541,0.707106781186554));
#7431=DIRECTION('',(-1.,0.,0.));
#7432=DIRECTION('',(1.,0.,0.));
#7433=DIRECTION('center_axis',(-0.923879532511291,0.,0.382683432365079));
#7434=DIRECTION('ref_axis',(0.382683432365079,0.,0.923879532511291));
#7435=DIRECTION('center_axis',(-0.707106781186548,0.,0.707106781186548));
#7436=DIRECTION('ref_axis',(0.5,0.707106781186547,0.5));
#7437=DIRECTION('',(0.707106781186548,0.,-0.707106781186548));
#7438=DIRECTION('',(-0.707106781186548,0.,0.707106781186548));
#7439=DIRECTION('center_axis',(-0.707106781186548,0.,-0.707106781186548));
#7440=DIRECTION('ref_axis',(-0.707106781186548,0.,0.707106781186548));
#7441=DIRECTION('',(0.,-1.,0.));
#7442=DIRECTION('',(0.707106781186548,0.,-0.707106781186548));
#7443=DIRECTION('',(0.,1.,0.));
#7444=DIRECTION('center_axis',(0.,0.,-1.));
#7445=DIRECTION('ref_axis',(1.,0.,0.));
#7446=DIRECTION('',(0.,1.,0.));
#7447=DIRECTION('',(1.,0.,0.));
#7448=DIRECTION('center_axis',(0.707106781186548,0.,-0.707106781186548));
#7449=DIRECTION('ref_axis',(-0.707106781186548,0.,-0.707106781186548));
#7450=DIRECTION('',(0.,-1.,0.));
#7451=DIRECTION('',(0.707106781186548,0.,0.707106781186548));
#7452=DIRECTION('center_axis',(1.,0.,0.));
#7453=DIRECTION('ref_axis',(0.,0.,1.));
#7454=DIRECTION('',(0.,1.,0.));
#7455=DIRECTION('',(0.,0.,1.));
#7456=DIRECTION('center_axis',(0.,-1.,0.));
#7457=DIRECTION('ref_axis',(-1.,0.,0.));
#7458=DIRECTION('center_axis',(0.,0.,1.));
#7459=DIRECTION('ref_axis',(0.707106781186548,-0.707106781186548,0.));
#7460=DIRECTION('',(0.,0.,-1.));
#7461=DIRECTION('center_axis',(0.382683432365099,8.20569863179165E-15,0.923879532511283));
#7462=DIRECTION('ref_axis',(0.923879532511283,1.98103089256172E-14,-0.382683432365098));
#7463=DIRECTION('center_axis',(-0.382683432365106,1.64113972635832E-14,
0.92387953251128));
#7464=DIRECTION('ref_axis',(-0.92387953251128,-3.96206178512373E-14,-0.382683432365105));
#7465=DIRECTION('center_axis',(-0.707106781186548,0.,-0.707106781186548));
#7466=DIRECTION('ref_axis',(0.499999999999999,-0.707106781186545,-0.500000000000005));
#7467=DIRECTION('',(-0.707106781186548,0.,-0.707106781186548));
#7468=DIRECTION('center_axis',(0.923879532511284,0.,0.382683432365097));
#7469=DIRECTION('ref_axis',(-0.382683432365097,0.,0.923879532511284));
#7470=DIRECTION('center_axis',(1.,0.,0.));
#7471=DIRECTION('ref_axis',(0.,-0.707106781186544,-0.707106781186551));
#7472=DIRECTION('',(-1.,0.,0.));
#7473=DIRECTION('center_axis',(0.923879532511287,0.,-0.38268343236509));
#7474=DIRECTION('ref_axis',(-0.38268343236509,0.,-0.923879532511287));
#7475=DIRECTION('center_axis',(-0.707106781186548,0.,0.707106781186548));
#7476=DIRECTION('ref_axis',(-0.5,-0.707106781186547,-0.5));
#7477=DIRECTION('',(-0.707106781186548,0.,0.707106781186548));
#7478=DIRECTION('center_axis',(0.382683432365092,0.,-0.923879532511286));
#7479=DIRECTION('ref_axis',(0.923879532511286,0.,0.382683432365091));
#7480=DIRECTION('center_axis',(0.,0.,-1.));
#7481=DIRECTION('ref_axis',(-0.707106781186548,-0.707106781186548,0.));
#7482=DIRECTION('',(0.,0.,-1.));
#7483=DIRECTION('',(0.,0.,1.));
#7484=DIRECTION('center_axis',(-0.382683432365106,0.,-0.92387953251128));
#7485=DIRECTION('ref_axis',(-0.92387953251128,0.,0.382683432365106));
#7486=DIRECTION('center_axis',(0.707106781186548,0.,0.707106781186548));
#7487=DIRECTION('ref_axis',(-0.5,-0.707106781186547,0.5));
#7488=DIRECTION('',(-0.707106781186548,0.,-0.707106781186548));
#7489=DIRECTION('',(0.707106781186548,0.,0.707106781186548));
#7490=DIRECTION('center_axis',(-0.923879532511283,0.,-0.382683432365099));
#7491=DIRECTION('ref_axis',(0.382683432365099,0.,-0.923879532511283));
#7492=DIRECTION('center_axis',(-1.,0.,0.));
#7493=DIRECTION('ref_axis',(0.,-0.707106781186554,0.707106781186541));
#7494=DIRECTION('',(-1.,0.,0.));
#7495=DIRECTION('',(1.,0.,0.));
#7496=DIRECTION('center_axis',(-0.923879532511283,0.,0.382683432365099));
#7497=DIRECTION('ref_axis',(0.382683432365099,0.,0.923879532511283));
#7498=DIRECTION('center_axis',(0.707106781186548,0.,-0.707106781186548));
#7499=DIRECTION('ref_axis',(0.5,-0.707106781186547,0.5));
#7500=DIRECTION('',(-0.707106781186548,0.,0.707106781186548));
#7501=DIRECTION('',(0.707106781186548,0.,-0.707106781186548));
#7502=DIRECTION('center_axis',(-0.707106781186548,0.,0.707106781186548));
#7503=DIRECTION('ref_axis',(0.707106781186548,0.,0.707106781186548));
#7504=DIRECTION('',(0.,-1.,0.));
#7505=DIRECTION('',(0.,1.,0.));
#7506=DIRECTION('center_axis',(0.,0.,1.));
#7507=DIRECTION('ref_axis',(-1.,0.,0.));
#7508=DIRECTION('',(0.,-1.,0.));
#7509=DIRECTION('center_axis',(0.707106781186548,0.,0.707106781186548));
#7510=DIRECTION('ref_axis',(0.707106781186548,0.,-0.707106781186548));
#7511=DIRECTION('center_axis',(0.,-1.,0.));
#7512=DIRECTION('ref_axis',(0.,0.,-1.));
#7513=DIRECTION('center_axis',(-1.,0.,0.));
#7514=DIRECTION('ref_axis',(0.,0.,-1.));
#9111=CARTESIAN_POINT('',(0.,0.,0.));
#9112=CARTESIAN_POINT('Origin',(21.2760503877808,-85.,85.));
#9113=CARTESIAN_POINT('',(18.2760503877808,-82.,85.));
#9114=CARTESIAN_POINT('Origin',(21.2760503877808,-82.,85.));
#9115=CARTESIAN_POINT('',(18.2760503877808,-66.,85.));
#9116=CARTESIAN_POINT('',(18.2760503877808,-85.,85.));
#9117=CARTESIAN_POINT('Origin',(21.2760503877808,-66.,85.));
#9118=CARTESIAN_POINT('Origin',(-20.7760503877808,-85.,85.));
#9119=CARTESIAN_POINT('',(-23.7760503877808,-82.,85.));
#9120=CARTESIAN_POINT('Origin',(-20.7760503877808,-82.,85.));
#9121=CARTESIAN_POINT('',(-23.7760503877808,-66.,85.));
#9122=CARTESIAN_POINT('',(-23.7760503877808,-85.,85.));
#9123=CARTESIAN_POINT('Origin',(-20.7760503877808,-66.,85.));
#9124=CARTESIAN_POINT('Origin',(-42.1783940322367,-82.,71.1256934864884));
#9125=CARTESIAN_POINT('',(-45.1783940322367,-82.,71.1256934864884));
#9126=CARTESIAN_POINT('Origin',(-42.1783940322367,-82.,71.1256934864884));
#9127=CARTESIAN_POINT('',(-45.1783940322367,-66.,71.1256934864884));
#9128=CARTESIAN_POINT('',(-45.1783940322367,-82.,71.1256934864884));
#9129=CARTESIAN_POINT('Origin',(-42.1783940322367,-66.,71.1256934864884));
#9130=CARTESIAN_POINT('Origin',(42.6783940322367,-82.,97.7923601531551));
#9131=CARTESIAN_POINT('',(39.6783940322367,-82.,97.7923601531551));
#9132=CARTESIAN_POINT('Origin',(42.6783940322367,-82.,97.7923601531551));
#9133=CARTESIAN_POINT('',(39.6783940322367,-66.,97.7923601531551));
#9134=CARTESIAN_POINT('',(39.6783940322367,-82.,97.7923601531551));
#9135=CARTESIAN_POINT('Origin',(42.6783940322367,-66.,97.7923601531551));
#9136=CARTESIAN_POINT('Origin',(42.6783940322367,-82.,71.1256934864884));
#9137=CARTESIAN_POINT('',(39.6783940322367,-82.,71.1256934864884));
#9138=CARTESIAN_POINT('Origin',(42.6783940322367,-82.,71.1256934864884));
#9139=CARTESIAN_POINT('',(39.6783940322367,-66.,71.1256934864884));
#9140=CARTESIAN_POINT('',(39.6783940322367,-82.,71.1256934864884));
#9141=CARTESIAN_POINT('Origin',(42.6783940322367,-66.,71.1256934864884));
#9142=CARTESIAN_POINT('Origin',(-42.1783940322367,-82.,97.7923601531551));
#9143=CARTESIAN_POINT('',(-45.1783940322367,-82.,97.7923601531551));
#9144=CARTESIAN_POINT('Origin',(-42.1783940322367,-82.,97.7923601531551));
#9145=CARTESIAN_POINT('',(-45.1783940322367,-66.,97.7923601531551));
#9146=CARTESIAN_POINT('',(-45.1783940322367,-82.,97.7923601531551));
#9147=CARTESIAN_POINT('Origin',(-42.1783940322367,-66.,97.7923601531551));
#9148=CARTESIAN_POINT('Origin',(-42.1783940322367,-82.,44.4590268198217));
#9149=CARTESIAN_POINT('',(-45.1783940322367,-82.,44.4590268198217));
#9150=CARTESIAN_POINT('Origin',(-42.1783940322367,-82.,44.4590268198217));
#9151=CARTESIAN_POINT('',(-45.1783940322367,-66.,44.4590268198217));
#9152=CARTESIAN_POINT('',(-45.1783940322367,-82.,44.4590268198217));
#9153=CARTESIAN_POINT('Origin',(-42.1783940322367,-66.,44.4590268198217));
#9154=CARTESIAN_POINT('Origin',(42.6783940322367,-82.,124.459026819822));
#9155=CARTESIAN_POINT('',(39.6783940322367,-82.,124.459026819822));
#9156=CARTESIAN_POINT('Origin',(42.6783940322367,-82.,124.459026819822));
#9157=CARTESIAN_POINT('',(39.6783940322367,-66.,124.459026819822));
#9158=CARTESIAN_POINT('',(39.6783940322367,-82.,124.459026819822));
#9159=CARTESIAN_POINT('Origin',(42.6783940322367,-66.,124.459026819822));
#9160=CARTESIAN_POINT('Origin',(42.6783940322367,-82.,44.4590268198217));
#9161=CARTESIAN_POINT('',(39.6783940322367,-82.,44.4590268198217));
#9162=CARTESIAN_POINT('Origin',(42.6783940322367,-82.,44.4590268198217));
#9163=CARTESIAN_POINT('',(39.6783940322367,-66.,44.4590268198217));
#9164=CARTESIAN_POINT('',(39.6783940322367,-82.,44.4590268198217));
#9165=CARTESIAN_POINT('Origin',(42.6783940322367,-66.,44.4590268198217));
#9166=CARTESIAN_POINT('Origin',(-42.1783940322367,-82.,124.459026819822));
#9167=CARTESIAN_POINT('',(-45.1783940322367,-82.,124.459026819822));
#9168=CARTESIAN_POINT('Origin',(-42.1783940322367,-82.,124.459026819822));
#9169=CARTESIAN_POINT('',(-45.1783940322367,-66.,124.459026819822));
#9170=CARTESIAN_POINT('',(-45.1783940322367,-82.,124.459026819822));
#9171=CARTESIAN_POINT('Origin',(-42.1783940322367,-66.,124.459026819822));
#9172=CARTESIAN_POINT('Origin',(49.5,-67.,60.));
#9173=CARTESIAN_POINT('',(50.5,-67.,130.));
#9174=CARTESIAN_POINT('',(50.5,-67.,40.));
#9175=CARTESIAN_POINT('',(50.5,-67.,60.));
#9176=CARTESIAN_POINT('',(49.5,-66.,40.4142135623731));
#9177=CARTESIAN_POINT('Origin',(49.5,-67.,40.4142135623731));
#9178=CARTESIAN_POINT('',(49.5,-66.,129.585786437627));
#9179=CARTESIAN_POINT('',(49.5,-66.,60.));
#9180=CARTESIAN_POINT('Origin',(49.5,-67.,129.585786437627));
#9181=CARTESIAN_POINT('Origin',(47.2928932188134,-67.,38.2071067811866));
#9182=CARTESIAN_POINT('',(45.5,-67.,35.));
#9183=CARTESIAN_POINT('',(48.,-67.,37.5));
#9184=CARTESIAN_POINT('',(45.0857864376269,-66.,36.));
#9185=CARTESIAN_POINT('Origin',(45.0857864376269,-67.,36.));
#9186=CARTESIAN_POINT('',(47.2928932188134,-66.,38.2071067811866));
#9187=CARTESIAN_POINT('Origin',(-24.5,-67.,36.));
#9188=CARTESIAN_POINT('',(-45.,-67.,35.));
#9189=CARTESIAN_POINT('',(-24.5,-67.,35.));
#9190=CARTESIAN_POINT('',(-44.5857864376269,-66.,36.));
#9191=CARTESIAN_POINT('Origin',(-44.5857864376269,-67.,36.));
#9192=CARTESIAN_POINT('',(-24.5,-66.,36.));
#9193=CARTESIAN_POINT('Origin',(-46.6678932188135,-67.,38.0821067811865));
#9194=CARTESIAN_POINT('',(-50.,-67.,40.));
#9195=CARTESIAN_POINT('',(-47.375,-67.,37.375));
#9196=CARTESIAN_POINT('',(-49.,-66.,40.4142135623731));
#9197=CARTESIAN_POINT('Origin',(-49.,-67.,40.4142135623731));
#9198=CARTESIAN_POINT('',(-46.6678932188135,-66.,38.0821067811865));
#9199=CARTESIAN_POINT('Origin',(-49.,-67.,110.));
#9200=CARTESIAN_POINT('',(-49.,-66.,129.585786437627));
#9201=CARTESIAN_POINT('',(-49.,-66.,110.));
#9202=CARTESIAN_POINT('',(-50.,-67.,130.));
#9203=CARTESIAN_POINT('',(-50.,-67.,110.));
#9204=CARTESIAN_POINT('Origin',(-49.,-67.,129.585786437627));
#9205=CARTESIAN_POINT('Origin',(-46.6678932188135,-67.,131.917893218813));
#9206=CARTESIAN_POINT('',(-44.5857864376269,-66.,134.));
#9207=CARTESIAN_POINT('',(-46.6678932188135,-66.,131.917893218813));
#9208=CARTESIAN_POINT('',(-45.,-67.,135.));
#9209=CARTESIAN_POINT('',(-47.375,-67.,132.625));
#9210=CARTESIAN_POINT('Origin',(-44.5857864376269,-67.,134.));
#9211=CARTESIAN_POINT('Origin',(25.5,-67.,134.));
#9212=CARTESIAN_POINT('',(45.0857864376269,-66.,134.));
#9213=CARTESIAN_POINT('',(25.5,-66.,134.));
#9214=CARTESIAN_POINT('',(45.5,-67.,135.));
#9215=CARTESIAN_POINT('',(25.5,-67.,135.));
#9216=CARTESIAN_POINT('Origin',(45.0857864376269,-67.,134.));
#9217=CARTESIAN_POINT('Origin',(47.2928932188134,-67.,131.792893218813));
#9218=CARTESIAN_POINT('',(48.,-67.,132.5));
#9219=CARTESIAN_POINT('',(47.2928932188134,-66.,131.792893218813));
#9220=CARTESIAN_POINT('Origin',(-47.5,-66.,37.5));
#9221=CARTESIAN_POINT('',(-45.,-81.,35.));
#9222=CARTESIAN_POINT('',(-45.,-66.,35.));
#9223=CARTESIAN_POINT('',(-50.,-81.,40.));
#9224=CARTESIAN_POINT('',(-47.375,-81.,37.375));
#9225=CARTESIAN_POINT('',(-50.,-66.,40.));
#9226=CARTESIAN_POINT('Origin',(-49.5,-66.,35.));
#9227=CARTESIAN_POINT('',(45.5,-81.,35.));
#9228=CARTESIAN_POINT('',(45.5,-66.,35.));
#9229=CARTESIAN_POINT('',(-24.5,-81.,35.));
#9230=CARTESIAN_POINT('Origin',(48.,-66.,37.5));
#9231=CARTESIAN_POINT('',(50.5,-81.,40.));
#9232=CARTESIAN_POINT('',(50.5,-66.,40.));
#9233=CARTESIAN_POINT('',(48.,-81.,37.5));
#9234=CARTESIAN_POINT('Origin',(50.5,-66.,35.));
#9235=CARTESIAN_POINT('',(50.5,-81.,130.));
#9236=CARTESIAN_POINT('',(50.5,-66.,130.));
#9237=CARTESIAN_POINT('',(50.5,-81.,60.));
#9238=CARTESIAN_POINT('Origin',(0.499999999999998,-66.,85.));
#9239=CARTESIAN_POINT('Origin',(49.5,-81.,60.));
#9240=CARTESIAN_POINT('',(49.5,-82.,129.585786437627));
#9241=CARTESIAN_POINT('',(49.5,-82.,40.4142135623731));
#9242=CARTESIAN_POINT('',(49.5,-82.,60.));
#9243=CARTESIAN_POINT('Origin',(49.5,-81.,40.4142135623731));
#9244=CARTESIAN_POINT('Origin',(49.5,-81.,129.585786437627));
#9245=CARTESIAN_POINT('Origin',(47.2928932188134,-81.,38.2071067811866));
#9246=CARTESIAN_POINT('',(45.0857864376269,-82.,36.));
#9247=CARTESIAN_POINT('',(47.2928932188134,-82.,38.2071067811866));
#9248=CARTESIAN_POINT('Origin',(45.0857864376269,-81.,36.));
#9249=CARTESIAN_POINT('Origin',(-24.5,-81.,36.));
#9250=CARTESIAN_POINT('',(-44.5857864376269,-82.,36.));
#9251=CARTESIAN_POINT('',(-24.5,-82.,36.));
#9252=CARTESIAN_POINT('Origin',(-44.5857864376269,-81.,36.));
#9253=CARTESIAN_POINT('Origin',(-46.6678932188135,-81.,38.0821067811865));
#9254=CARTESIAN_POINT('',(-49.,-82.,40.4142135623731));
#9255=CARTESIAN_POINT('',(-46.6678932188135,-82.,38.0821067811865));
#9256=CARTESIAN_POINT('Origin',(-49.,-81.,40.4142135623731));
#9257=CARTESIAN_POINT('Origin',(-49.,-81.,110.));
#9258=CARTESIAN_POINT('',(-50.,-81.,130.));
#9259=CARTESIAN_POINT('',(-50.,-81.,110.));
#9260=CARTESIAN_POINT('',(-49.,-82.,129.585786437627));
#9261=CARTESIAN_POINT('',(-49.,-82.,110.));
#9262=CARTESIAN_POINT('Origin',(-49.,-81.,129.585786437627));
#9263=CARTESIAN_POINT('Origin',(-46.6678932188135,-81.,131.917893218813));
#9264=CARTESIAN_POINT('',(-45.,-81.,135.));
#9265=CARTESIAN_POINT('',(-47.375,-81.,132.625));
#9266=CARTESIAN_POINT('',(-44.5857864376269,-82.,134.));
#9267=CARTESIAN_POINT('',(-46.6678932188135,-82.,131.917893218813));
#9268=CARTESIAN_POINT('Origin',(-44.5857864376269,-81.,134.));
#9269=CARTESIAN_POINT('Origin',(25.5,-81.,134.));
#9270=CARTESIAN_POINT('',(45.5,-81.,135.));
#9271=CARTESIAN_POINT('',(25.5,-81.,135.));
#9272=CARTESIAN_POINT('',(45.0857864376269,-82.,134.));
#9273=CARTESIAN_POINT('',(25.5,-82.,134.));
#9274=CARTESIAN_POINT('Origin',(45.0857864376269,-81.,134.));
#9275=CARTESIAN_POINT('Origin',(47.2928932188134,-81.,131.792893218813));
#9276=CARTESIAN_POINT('',(48.,-81.,132.5));
#9277=CARTESIAN_POINT('',(47.2928932188134,-82.,131.792893218813));
#9278=CARTESIAN_POINT('Origin',(-47.5,-66.,132.5));
#9279=CARTESIAN_POINT('',(-50.,-66.,130.));
#9280=CARTESIAN_POINT('',(-45.,-66.,135.));
#9281=CARTESIAN_POINT('Origin',(50.5,-66.,135.));
#9282=CARTESIAN_POINT('',(45.5,-66.,135.));
#9283=CARTESIAN_POINT('Origin',(48.,-66.,132.5));
#9284=CARTESIAN_POINT('Origin',(0.499999999999998,-82.,85.));
#9285=CARTESIAN_POINT('Origin',(-50.,-66.,135.));
#10113=UNCERTAINTY_MEASURE_WITH_UNIT(LENGTH_MEASURE(0.01),#10132,
'DISTANCE_ACCURACY_VALUE',
'Maximum model space distance between geometric entities at asserted c
onnectivities');
#10119=UNCERTAINTY_MEASURE_WITH_UNIT(LENGTH_MEASURE(0.01),#10132,
'DISTANCE_ACCURACY_VALUE',
'Maximum model space distance between geometric entities at asserted c
onnectivities');
#10125=(
GEOMETRIC_REPRESENTATION_CONTEXT(3)
GLOBAL_UNCERTAINTY_ASSIGNED_CONTEXT((#10113))
GLOBAL_UNIT_ASSIGNED_CONTEXT((#10132,#10134,#10135))
REPRESENTATION_CONTEXT('','3D')
);
#10131=(
GEOMETRIC_REPRESENTATION_CONTEXT(3)
GLOBAL_UNCERTAINTY_ASSIGNED_CONTEXT((#10119))
GLOBAL_UNIT_ASSIGNED_CONTEXT((#10132,#10134,#10135))
REPRESENTATION_CONTEXT('','3D')
);
#10132=(
LENGTH_UNIT()
NAMED_UNIT(*)
SI_UNIT(.MILLI.,.METRE.)
);
#10134=(
NAMED_UNIT(*)
PLANE_ANGLE_UNIT()
SI_UNIT($,.RADIAN.)
);
#10135=(
NAMED_UNIT(*)
SI_UNIT($,.STERADIAN.)
SOLID_ANGLE_UNIT()
);
#10141=SHAPE_DEFINITION_REPRESENTATION(#10152,#10173);
#10152=PRODUCT_DEFINITION_SHAPE('',$,#10185);
#10173=SHAPE_REPRESENTATION('',(#6236),#10125);
#10179=PRODUCT_DEFINITION_CONTEXT('part definition',#10214,'design');
#10185=PRODUCT_DEFINITION('Front_Block_02','Front_Block_02',#10196,#10179);
#10196=PRODUCT_DEFINITION_FORMATION('',$,#10221);
#10214=APPLICATION_CONTEXT(
'Core Data for Automotive Mechanical Design Process');
#10215=PRODUCT_CONTEXT('part definition',#10214,'mechanical');
#10221=PRODUCT('Front_Block_02','Front_Block_02',$,(#10215));
#10241=COLOUR_RGB('Dark Blue',0.08,0.2,0.34);
#10242=FILL_AREA_STYLE_COLOUR('',#10241);
#10243=FILL_AREA_STYLE('',(#10242));
#10244=SURFACE_STYLE_FILL_AREA(#10243);
#10245=SURFACE_SIDE_STYLE('',(#10244));
#10246=SURFACE_STYLE_USAGE(.BOTH.,#10245);
#10247=PRESENTATION_STYLE_ASSIGNMENT((#10246));
ENDSEC;
END-ISO-10303-21;
